ISO-10303-21;
HEADER;
FILE_DESCRIPTION (('STEP AP203'),
    '1' );
FILE_NAME ('1602p_c_08.step',
    '2026-10-31T14:11:27',
    ( '' ),
    ( '' ),
    'SwSTEP 2.0',
    'SolidWorks 2024',
    '' );
FILE_SCHEMA (( 'AUTOMOTIVE_DESIGN' ));
ENDSEC;

DATA;
#6=ORIENTED_EDGE ( 'NONE', *, *, #3696, .T. ) ;
#17=ORIENTED_EDGE ( 'NONE', *, *, #3530, .T. ) ;
#19=ADVANCED_FACE ( 'NONE', ( #17012 ), #726, .F. ) ;
#25=EDGE_LOOP ( 'NONE', ( #13896, #19645, #1071, #1606 ) ) ;
#28=ORIENTED_EDGE ( 'NONE', *, *, #3722, .T. ) ;
#37=VECTOR ( 'NONE', #8550, 1000.000000000000000 ) ;
#72=DIRECTION ( 'NONE',  ( -0.9999862922474493931, -0.005235963827110373843, 0.000000000000000000 ) ) ;
#136=FACE_OUTER_BOUND ( 'NONE', #13808, .T. ) ;
#245=CARTESIAN_POINT ( 'NONE',  ( -19.49999999982379961, -0.1021026942259709996, 9.160072195675308484E-14 ) ) ;
#372=ORIENTED_EDGE ( 'NONE', *, *, #22651, .T. ) ;
#415=DIRECTION ( 'NONE',  ( 1.000000000000000000, 0.000000000000000000, 0.000000000000000000 ) ) ;
#425=DIRECTION ( 'NONE',  ( 1.000000000000000000, -1.466984912809900042E-16, -5.345529420184390105E-52 ) ) ;
#428=LINE ( 'NONE', #13156, #1760 ) ;
#431=CARTESIAN_POINT ( 'NONE',  ( -30.79248430819439974, 6.338858557519089665, 2.999000000000090260 ) ) ;
#489=VERTEX_POINT ( 'NONE', #1847 ) ;
#553=LINE ( 'NONE', #20395, #17489 ) ;
#598=CIRCLE ( 'NONE', #13894, 3.499999999999998224 ) ;
#602=LINE ( 'NONE', #4309, #22373 ) ;
#642=ORIENTED_EDGE ( 'NONE', *, *, #16160, .T. ) ;
#656=ADVANCED_FACE ( 'NONE', ( #11261 ), #13251, .F. ) ;
#664=VECTOR ( 'NONE', #5401, 1000.000000000000114 ) ;
#726=PLANE ( 'NONE',  #19683 ) ;
#734=CYLINDRICAL_SURFACE ( 'NONE', #5234, 6.499999999999997335 ) ;
#747=VERTEX_POINT ( 'NONE', #18608 ) ;
#783=EDGE_CURVE ( 'NONE', #5737, #19582, #7671, .T. ) ;
#872=AXIS2_PLACEMENT_3D ( 'NONE', #8546, #19572, #23111 ) ;
#974=DIRECTION ( 'NONE',  ( -0.9999862922474492821, -0.005235963827121953122, 1.466966272682004590E-16 ) ) ;
#1015=DIRECTION ( 'NONE',  ( -0.005235963827121951387, 0.9999862922474492821, 7.400535959139851804E-19 ) ) ;
#1058=DIRECTION ( 'NONE',  ( -0.9999862922474492821, -0.005235963827121951387, 1.466966272682004590E-16 ) ) ;
#1071=ORIENTED_EDGE ( 'NONE', *, *, #16968, .T. ) ;
#1086=DIRECTION ( 'NONE',  ( 0.005235963827101452160, -0.9999862922474493931, 5.479105319409471602E-16 ) ) ;
#1096=FACE_OUTER_BOUND ( 'NONE', #15890, .T. ) ;
#1103=ORIENTED_EDGE ( 'NONE', *, *, #9591, .F. ) ;
#1164=CARTESIAN_POINT ( 'NONE',  ( -28.45655959278310121, -6.649088660734180145, 0.7325259402522749097 ) ) ;
#1208=VECTOR ( 'NONE', #1015, 1000.000000000000114 ) ;
#1257=VERTEX_POINT ( 'NONE', #4196 ) ;
#1306=PRODUCT_DEFINITION_SHAPE ( 'NONE', 'NONE',  #13884 ) ;
#1313=FACE_BOUND ( 'NONE', #16135, .T. ) ;
#1397=EDGE_CURVE ( 'NONE', #14820, #13595, #4448, .T. ) ;
#1451=CARTESIAN_POINT ( 'NONE',  ( -72.77122628570259621, -6.881121833202230142, -0.01852613985921119921 ) ) ;
#1592=AXIS2_PLACEMENT_3D ( 'NONE', #2985, #8583, #4773 ) ;
#1606=ORIENTED_EDGE ( 'NONE', *, *, #18199, .T. ) ;
#1614=ORIENTED_EDGE ( 'NONE', *, *, #15520, .F. ) ;
#1753=ORIENTED_EDGE ( 'NONE', *, *, #15494, .F. ) ;
#1760=VECTOR ( 'NONE', #14465, 1000.000000000000000 ) ;
#1827=EDGE_CURVE ( 'NONE', #7573, #5643, #23134, .T. ) ;
#1847=CARTESIAN_POINT ( 'NONE',  ( -0.03403376487617929685, 6.499910899608420500, 8.874490886070419291E-14 ) ) ;
#1863=EDGE_CURVE ( 'NONE', #2098, #22438, #8594, .T. ) ;
#1937=CARTESIAN_POINT ( 'NONE',  ( 3.499952022866072543, 0.01832587339492582068, 8.822666031689207903E-14 ) ) ;
#1962=CARTESIAN_POINT ( 'NONE',  ( -30.72441677844210162, -6.660963241697119841, 2.999000000000090260 ) ) ;
#1992=DIRECTION ( 'NONE',  ( 0.005235963827101452160, -0.9999862922474493931, 5.479105319409471602E-16 ) ) ;
#2020=ORIENTED_EDGE ( 'NONE', *, *, #3611, .T. ) ;
#2040=DIRECTION ( 'NONE',  ( 0.000000000000000000, 0.000000000000000000, -1.000000000000000000 ) ) ;
#2065=DIRECTION ( 'NONE',  ( 0.005235963827101446956, -0.9999862922474495042, 5.479105319409467658E-16 ) ) ;
#2083=EDGE_CURVE ( 'NONE', #12797, #6625, #598, .T. ) ;
#2086=CARTESIAN_POINT ( 'NONE',  ( -26.75688440168130100, 6.359989102302520791, 2.500292893218799772 ) ) ;
#2098=VERTEX_POINT ( 'NONE', #10705 ) ;
#2127=DIRECTION ( 'NONE',  ( 0.005235963827101446956, -0.9999862922474495042, 5.479105319409467658E-16 ) ) ;
#2148=SHAPE_REPRESENTATION_RELATIONSHIP ( 'NONE' , 'NONE' ,  #20817, #11367 ) ;
#2216=ORIENTED_EDGE ( 'NONE', *, *, #8255, .T. ) ;
#2345=LINE ( 'NONE', #8051, #1208 ) ;
#2374=ORIENTED_EDGE ( 'NONE', *, *, #5600, .F. ) ;
#2391=CARTESIAN_POINT ( 'NONE',  ( 1.358598381910800010E-16, -1.434096706618689895E-15, 8.874009851233079243E-14 ) ) ;
#2406=ORIENTED_EDGE ( 'NONE', *, *, #6355, .T. ) ;
#2464=LINE ( 'NONE', #8162, #21625 ) ;
#2488=ORIENTED_EDGE ( 'NONE', *, *, #23166, .F. ) ;
#2490=ORIENTED_EDGE ( 'NONE', *, *, #10150, .F. ) ;
#2535=DIRECTION ( 'NONE',  ( -1.466984912809907930E-16, -2.805478249466190329E-20, -1.000000000000000000 ) ) ;
#2569=CARTESIAN_POINT ( 'NONE',  ( 0.000000000000000000, 0.000000000000000000, 0.000000000000000000 ) ) ;
#2610=CARTESIAN_POINT ( 'NONE',  ( -30.75845054331819739, -0.1610523420890289936, 2.999000000000090260 ) ) ;
#2645=DIRECTION ( 'NONE',  ( -0.7070970883417637687, -0.003702385528197199398, -0.7071067811865480168 ) ) ;
#2679=ADVANCED_FACE ( 'NONE', ( #1096 ), #13586, .T. ) ;
#2689=DIRECTION ( 'NONE',  ( 4.115594265198981899E-36, 2.805478249476870212E-20, 1.000000000000000000 ) ) ;
#2724=CARTESIAN_POINT ( 'NONE',  ( -22.99995202268987171, -0.1204285676208978334, 2.500000000000090594 ) ) ;
#2746=AXIS2_PLACEMENT_3D ( 'NONE', #15981, #23093, #21331 ) ;
#2787=DIRECTION ( 'NONE',  ( 0.000000000000000000, -2.538189087996114879E-14, -1.000000000000000000 ) ) ;
#2985=CARTESIAN_POINT ( 'NONE',  ( -26.72214353971689960, -0.1399180949200579949, 2.500999999999910184 ) ) ;
#3071=ORIENTED_EDGE ( 'NONE', *, *, #1827, .T. ) ;
#3079=VERTEX_POINT ( 'NONE', #4389 ) ;
#3181=VECTOR ( 'NONE', #11999, 1000.000000000000114 ) ;
#3220=VECTOR ( 'NONE', #22894, 1000.000000000000000 ) ;
#3297=EDGE_CURVE ( 'NONE', #15392, #6625, #428, .T. ) ;
#3307=DIRECTION ( 'NONE',  ( -0.005235963827102643048, 0.9999862922474495042, -7.723249237701186312E-15 ) ) ;
#3341=ORIENTED_EDGE ( 'NONE', *, *, #15306, .T. ) ;
#3398=DIRECTION ( 'NONE',  ( -0.9999862922474492821, -0.005235963827121951387, 1.466966272682004590E-16 ) ) ;
#3408=ORIENTED_EDGE ( 'NONE', *, *, #9230, .F. ) ;
#3419=LINE ( 'NONE', #14469, #6961 ) ;
#3469=ORIENTED_EDGE ( 'NONE', *, *, #12340, .F. ) ;
#3530=EDGE_CURVE ( 'NONE', #14820, #22403, #13268, .T. ) ;
#3539=FACE_OUTER_BOUND ( 'NONE', #17262, .T. ) ;
#3578=PLANE ( 'NONE',  #12307 ) ;
#3582=DIRECTION ( 'NONE',  ( 0.000000000000000000, -2.739767185169287006E-14, -1.000000000000000000 ) ) ;
#3611=EDGE_CURVE ( 'NONE', #747, #11532, #553, .T. ) ;
#3662=LINE ( 'NONE', #5110, #7697 ) ;
#3681=VERTEX_POINT ( 'NONE', #8633 ) ;
#3696=EDGE_CURVE ( 'NONE', #15392, #18750, #16707, .T. ) ;
#3722=EDGE_CURVE ( 'NONE', #12473, #489, #17542, .T. ) ;
#3739=ORIENTED_EDGE ( 'NONE', *, *, #16968, .F. ) ;
#3806=( NAMED_UNIT ( * ) SI_UNIT ( $, .STERADIAN. ) SOLID_ANGLE_UNIT ( ) );
#3815=CARTESIAN_POINT ( 'NONE',  ( -69.90454993788389970, 6.134066389438220135, -0.7502499999999080460 ) ) ;
#3880=DIRECTION ( 'NONE',  ( 1.466984912809909902E-16, 2.805478249466310097E-20, 1.000000000000000000 ) ) ;
#3905=VECTOR ( 'NONE', #12160, 999.9999999999998863 ) ;
#3914=CIRCLE ( 'NONE', #872, 3.499999999999998668 ) ;
#3970=FACE_OUTER_BOUND ( 'NONE', #10489, .T. ) ;
#4102=DIRECTION ( 'NONE',  ( -0.9999862922474492821, -0.005235963827121951387, 1.466966272682004590E-16 ) ) ;
#4121=PLANE ( 'NONE',  #5765 ) ;
#4138=VECTOR ( 'NONE', #7903, 1000.000000000000114 ) ;
#4139=EDGE_CURVE ( 'NONE', #1257, #16889, #19525, .T. ) ;
#4196=CARTESIAN_POINT ( 'NONE',  ( -28.52462712253550237, 6.350733138482030249, 0.7325259402521719920 ) ) ;
#4206=LINE ( 'NONE', #9803, #10423 ) ;
#4241=DIRECTION ( 'NONE',  ( 0.005235963827102643048, -0.9999862922474495042, 7.723249237701186312E-15 ) ) ;
#4309=CARTESIAN_POINT ( 'NONE',  ( -69.83648240813081998, -6.865755409778439677, -0.01852613985921119921 ) ) ;
#4330=CARTESIAN_POINT ( 'NONE',  ( -30.79248430819439974, 6.338858557519069237, 2.999000000000090260 ) ) ;
#4359=CARTESIAN_POINT ( 'NONE',  ( 3.499952022866073431, 0.01832587339492582415, 2.500000000000089706 ) ) ;
#4361=ORIENTED_EDGE ( 'NONE', *, *, #9591, .T. ) ;
#4379=AXIS2_PLACEMENT_3D ( 'NONE', #23057, #7372, #18050 ) ;
#4389=CARTESIAN_POINT ( 'NONE',  ( -30.72441677844230057, -6.660963241697680282, 3.000000000000090150 ) ) ;
#4448=CIRCLE ( 'NONE', #19248, 0.0009999999999225038516 ) ;
#4477=EDGE_LOOP ( 'NONE', ( #17805, #5906, #642, #11314 ) ) ;
#4582=ADVANCED_FACE ( 'NONE', ( #22337 ), #13336, .F. ) ;
#4650=ORIENTED_EDGE ( 'NONE', *, *, #8255, .F. ) ;
#4730=LINE ( 'NONE', #14103, #3220 ) ;
#4749=EDGE_CURVE ( 'NONE', #22247, #16889, #15268, .T. ) ;
#4760=CARTESIAN_POINT ( 'NONE',  ( -28.95596696049959817, -6.651703575491109355, 4.767474059747909720 ) ) ;
#4763=CIRCLE ( 'NONE', #10860, 0.0009999999996440807337 ) ;
#4773=DIRECTION ( 'NONE',  ( 0.000000000000000000, -2.710505431696529444E-14, -1.000000000000000000 ) ) ;
#4786=FACE_OUTER_BOUND ( 'NONE', #11202, .T. ) ;
#4919=PRODUCT ( '1602p_c_08', '1602p_c_08', '', ( #15428 ) ) ;
#4942=DESIGN_CONTEXT ( 'detailed design', #19912, 'design' ) ;
#5110=CARTESIAN_POINT ( 'NONE',  ( -70.63306599754589854, 6.130251853413639651, 5.500000000000099476 ) ) ;
#5129=DIRECTION ( 'NONE',  ( -0.005235963827121952255, 0.9999862922474493931, -2.738476122049126182E-14 ) ) ;
#5150=ORIENTED_EDGE ( 'NONE', *, *, #9230, .T. ) ;
#5151=CARTESIAN_POINT ( 'NONE',  ( 1.133770560463819718E-13, -8.411617717272179750E-16, 8.874009851233079243E-14 ) ) ;
#5203=CARTESIAN_POINT ( 'NONE',  ( 0.03403376487640599746, -6.499910899608420500, 8.873528816395729098E-14 ) ) ;
#5214=EDGE_LOOP ( 'NONE', ( #23074, #15099, #17, #17124 ) ) ;
#5234=AXIS2_PLACEMENT_3D ( 'NONE', #8009, #7539, #11479 ) ;
#5303=VECTOR ( 'NONE', #7908, 1000.000000000000114 ) ;
#5345=EDGE_CURVE ( 'NONE', #22438, #2098, #6461, .T. ) ;
#5401=DIRECTION ( 'NONE',  ( -0.7070970883417637687, -0.003702385528188433840, 0.7071067811865477948 ) ) ;
#5448=ORIENTED_EDGE ( 'NONE', *, *, #3722, .F. ) ;
#5452=ORIENTED_EDGE ( 'NONE', *, *, #9286, .T. ) ;
#5486=CARTESIAN_POINT ( 'NONE',  ( -26.68810977484059777, -6.639828994528159889, 2.501000000000090484 ) ) ;
#5502=VERTEX_POINT ( 'NONE', #6465 ) ;
#5600=EDGE_CURVE ( 'NONE', #13305, #5502, #20614, .T. ) ;
#5610=LINE ( 'NONE', #12856, #18684 ) ;
#5635=VECTOR ( 'NONE', #3880, 1000.000000000000000 ) ;
#5643=VERTEX_POINT ( 'NONE', #23073 ) ;
#5670=DIRECTION ( 'NONE',  ( 1.466984912809907930E-16, 2.805478249466195144E-20, 1.000000000000000000 ) ) ;
#5714=CARTESIAN_POINT ( 'NONE',  ( -26.68881687192900287, -6.639832696913689603, 2.500292893218899692 ) ) ;
#5716=CLOSED_SHELL ( 'NONE', ( #656, #22688, #2679, #14449, #21742, #10124, #11676, #7392, #12455, #19, #4582, #15729, #14673, #20056, #12454, #17543, #15742, #13285 ) ) ;
#5737=VERTEX_POINT ( 'NONE', #19412 ) ;
#5765=AXIS2_PLACEMENT_3D ( 'NONE', #22597, #6950, #17748 ) ;
#5767=ORIENTED_EDGE ( 'NONE', *, *, #8368, .F. ) ;
#5826=FACE_OUTER_BOUND ( 'NONE', #5214, .T. ) ;
#5906=ORIENTED_EDGE ( 'NONE', *, *, #5600, .T. ) ;
#5907=LINE ( 'NONE', #20393, #8994 ) ;
#5918=DIRECTION ( 'NONE',  ( -0.9999862922474492821, -0.005235963827121953122, 1.239088197126291310E-16 ) ) ;
#6019=ORIENTED_EDGE ( 'NONE', *, *, #3696, .F. ) ;
#6072=DIRECTION ( 'NONE',  ( -0.005235963827102643048, 0.9999862922474495042, -7.723249237701186312E-15 ) ) ;
#6134=CARTESIAN_POINT ( 'NONE',  ( 0.03403376487640599746, -6.499910899608420500, 8.873528816395729098E-14 ) ) ;
#6138=DIRECTION ( 'NONE',  ( 0.9999862922474493931, 0.005235963827101436548, -1.466966272681988813E-16 ) ) ;
#6168=CIRCLE ( 'NONE', #9612, 3.499999999999998224 ) ;
#6187=CARTESIAN_POINT ( 'NONE',  ( -22.99995202268987171, -0.1204285676208978334, 9.211416015219178562E-14 ) ) ;
#6221=DIRECTION ( 'NONE',  ( -0.7071116276255479116, 0.000000000000000000, 0.7071019347143299161 ) ) ;
#6287=ORIENTED_EDGE ( 'NONE', *, *, #4749, .T. ) ;
#6310=ORIENTED_EDGE ( 'NONE', *, *, #18199, .F. ) ;
#6355=EDGE_CURVE ( 'NONE', #1257, #14820, #9283, .T. ) ;
#6362=AXIS2_PLACEMENT_3D ( 'NONE', #245, #14750, #21977 ) ;
#6372=VECTOR ( 'NONE', #15837, 1000.000000000000000 ) ;
#6461=CIRCLE ( 'NONE', #16272, 3.499999999999998668 ) ;
#6465=CARTESIAN_POINT ( 'NONE',  ( -30.72441677844230057, -6.660963241697680282, 5.500000000000089706 ) ) ;
#6502=ORIENTED_EDGE ( 'NONE', *, *, #2083, .T. ) ;
#6511=CARTESIAN_POINT ( 'NONE',  ( -30.72441677844230057, -6.660963241697680282, 3.000000000000090150 ) ) ;
#6577=LINE ( 'NONE', #17843, #3905 ) ;
#6586=DIRECTION ( 'NONE',  ( 0.000000000000000000, 0.000000000000000000, -1.000000000000000000 ) ) ;
#6625=VERTEX_POINT ( 'NONE', #6187 ) ;
#6631=ORIENTED_EDGE ( 'NONE', *, *, #21080, .T. ) ;
#6705=CARTESIAN_POINT ( 'NONE',  ( -16.00004797695773107, -0.08377682083104374955, 9.108728376131438406E-14 ) ) ;
#6829=DIRECTION ( 'NONE',  ( -0.005235963827121941846, 0.9999862922474492821, 7.400535959148351896E-19 ) ) ;
#6875=PRODUCT_DEFINITION_FORMATION_WITH_SPECIFIED_SOURCE ( 'ANY', '', #4919, .NOT_KNOWN. ) ;
#6921=AXIS2_PLACEMENT_3D ( 'NONE', #17895, #15765, #3398 ) ;
#6950=DIRECTION ( 'NONE',  ( 4.115594265186587621E-36, 2.805478249468460519E-20, 1.000000000000000000 ) ) ;
#6961=VECTOR ( 'NONE', #3307, 999.9999999999998863 ) ;
#7006=EDGE_CURVE ( 'NONE', #13450, #8538, #3662, .T. ) ;
#7080=CARTESIAN_POINT ( 'NONE',  ( -26.68810977484059777, -6.639828994528159889, 9.265539023039960360E-14 ) ) ;
#7083=EDGE_CURVE ( 'NONE', #18750, #15392, #6168, .T. ) ;
#7310=CARTESIAN_POINT ( 'NONE',  ( -28.45655959278310121, -6.649088660734180145, 0.7325259402522749097 ) ) ;
#7351=DIRECTION ( 'NONE',  ( 0.000000000000000000, -2.738683416504465444E-14, -1.000000000000000000 ) ) ;
#7372=DIRECTION ( 'NONE',  ( -0.005235963827121952255, 0.9999862922474493931, -2.738476122049126182E-14 ) ) ;
#7392=ADVANCED_FACE ( 'NONE', ( #17875 ), #20006, .T. ) ;
#7405=DIRECTION ( 'NONE',  ( -0.005235963827197880234, 0.9999862922474489491, 6.376474323085884347E-17 ) ) ;
#7436=VERTEX_POINT ( 'NONE', #14200 ) ;
#7440=DIRECTION ( 'NONE',  ( 0.000000000000000000, -6.936119456124777094E-16, -1.000000000000000000 ) ) ;
#7442=DIRECTION ( 'NONE',  ( -0.9999862922474492821, -0.005235963827121951387, 1.466966272682004590E-16 ) ) ;
#7445=EDGE_CURVE ( 'NONE', #5643, #13084, #12662, .T. ) ;
#7452=CARTESIAN_POINT ( 'NONE',  ( -69.83648240813081998, -6.865755409778316221, 5.500000000000099476 ) ) ;
#7516=CIRCLE ( 'NONE', #15452, 0.0009999999999975306419 ) ;
#7539=DIRECTION ( 'NONE',  ( -1.466984912809909902E-16, -2.805478249466335375E-20, -1.000000000000000000 ) ) ;
#7567=PLANE ( 'NONE',  #20001 ) ;
#7573=VERTEX_POINT ( 'NONE', #7887 ) ;
#7626=DIRECTION ( 'NONE',  ( -0.005235963827101446089, 0.9999862922474493931, 7.400535959109775519E-19 ) ) ;
#7646=LINE ( 'NONE', #16431, #16574 ) ;
#7671=LINE ( 'NONE', #2086, #5303 ) ;
#7697=VECTOR ( 'NONE', #18250, 1000.000000000000000 ) ;
#7723=CIRCLE ( 'NONE', #16758, 2.500999999999919954 ) ;
#7731=ORIENTED_EDGE ( 'NONE', *, *, #22977, .F. ) ;
#7798=CARTESIAN_POINT ( 'NONE',  ( -26.75617730459320143, 6.359992804688050505, 2.500999999999740098 ) ) ;
#7854=AXIS2_PLACEMENT_3D ( 'NONE', #3815, #7405, #14637 ) ;
#7861=LINE ( 'NONE', #5714, #15175 ) ;
#7873=ORIENTED_EDGE ( 'NONE', *, *, #1397, .T. ) ;
#7885=CIRCLE ( 'NONE', #14322, 3.499999999999998668 ) ;
#7887=CARTESIAN_POINT ( 'NONE',  ( -26.68810977484059777, -6.639828994528159889, 2.500000000000090150 ) ) ;
#7888=PLANE ( 'NONE',  #12819 ) ;
#7903=DIRECTION ( 'NONE',  ( 0.9999862922474493931, 0.005235963827101436548, -1.466966272681988813E-16 ) ) ;
#7908=DIRECTION ( 'NONE',  ( -0.7070970883417637687, -0.003702385528188433840, 0.7071067811865477948 ) ) ;
#8009=CARTESIAN_POINT ( 'NONE',  ( 1.133770560463819718E-13, -8.411617717272179750E-16, 8.874009851233079243E-14 ) ) ;
#8051=CARTESIAN_POINT ( 'NONE',  ( -26.68810977484059777, -6.639828994528159889, 9.265539023039960360E-14 ) ) ;
#8056=ORIENTED_EDGE ( 'NONE', *, *, #15520, .T. ) ;
#8057=ORIENTED_EDGE ( 'NONE', *, *, #22462, .T. ) ;
#8115=CARTESIAN_POINT ( 'NONE',  ( -30.72441677844230057, -6.660963241697680282, 5.500000000000089706 ) ) ;
#8162=CARTESIAN_POINT ( 'NONE',  ( 3.499952022866071211, 0.01832587339492581721, 8.822666031689207903E-14 ) ) ;
#8164=PLANE ( 'NONE',  #8617 ) ;
#8165=DIRECTION ( 'NONE',  ( 0.005235963827104182615, -0.9999862922474495042, -7.400535959113083303E-19 ) ) ;
#8173=ORIENTED_EDGE ( 'NONE', *, *, #18283, .T. ) ;
#8201=ORIENTED_EDGE ( 'NONE', *, *, #21811, .F. ) ;
#8255=EDGE_CURVE ( 'NONE', #12003, #13977, #3914, .T. ) ;
#8330=CARTESIAN_POINT ( 'NONE',  ( -30.79177721110609767, 6.338862259904598950, 2.999707106781179800 ) ) ;
#8368=EDGE_CURVE ( 'NONE', #3079, #13595, #22897, .T. ) ;
#8536=FACE_OUTER_BOUND ( 'NONE', #16776, .T. ) ;
#8538=VERTEX_POINT ( 'NONE', #21570 ) ;
#8546=CARTESIAN_POINT ( 'NONE',  ( 5.026060663935580067E-16, -1.434026569662460006E-15, 2.500000000000090150 ) ) ;
#8550=DIRECTION ( 'NONE',  ( 1.466984912809909902E-16, 2.805478249466310097E-20, 1.000000000000000000 ) ) ;
#8583=DIRECTION ( 'NONE',  ( -0.005235963827121952255, 0.9999862922474493931, -2.738476122049126182E-14 ) ) ;
#8594=CIRCLE ( 'NONE', #13517, 3.499999999999998668 ) ;
#8599=LINE ( 'NONE', #6705, #6372 ) ;
#8617=AXIS2_PLACEMENT_3D ( 'NONE', #18623, #16694, #425 ) ;
#8633=CARTESIAN_POINT ( 'NONE',  ( 0.03403376487640639991, -6.499910899608420500, 2.500000000000090150 ) ) ;
#8660=ORIENTED_EDGE ( 'NONE', *, *, #6355, .F. ) ;
#8691=FACE_BOUND ( 'NONE', #14294, .T. ) ;
#8698=VERTEX_POINT ( 'NONE', #13499 ) ;
#8806=ORIENTED_EDGE ( 'NONE', *, *, #23469, .F. ) ;
#8813=ORIENTED_EDGE ( 'NONE', *, *, #23166, .T. ) ;
#8898=CARTESIAN_POINT ( 'NONE',  ( -0.03403376487617929685, 6.499910899608420500, 8.874490886070419291E-14 ) ) ;
#8994=VECTOR ( 'NONE', #6138, 1000.000000000000114 ) ;
#9008=ORIENTED_EDGE ( 'NONE', *, *, #1827, .F. ) ;
#9230=EDGE_CURVE ( 'NONE', #747, #13595, #4206, .T. ) ;
#9283=LINE ( 'NONE', #10850, #13047 ) ;
#9286=EDGE_CURVE ( 'NONE', #747, #8538, #17743, .T. ) ;
#9296=FACE_OUTER_BOUND ( 'NONE', #18402, .T. ) ;
#9318=CARTESIAN_POINT ( 'NONE',  ( -30.72441677844210162, -6.660963241697129611, 2.999000000000090260 ) ) ;
#9341=ORIENTED_EDGE ( 'NONE', *, *, #16029, .F. ) ;
#9380=ORIENTED_EDGE ( 'NONE', *, *, #5345, .T. ) ;
#9414=ORIENTED_EDGE ( 'NONE', *, *, #22775, .T. ) ;
#9527=VECTOR ( 'NONE', #11984, 1000.000000000000114 ) ;
#9591=EDGE_CURVE ( 'NONE', #13305, #11532, #602, .T. ) ;
#9612=AXIS2_PLACEMENT_3D ( 'NONE', #22292, #5670, #5918 ) ;
#9662=MANIFOLD_SOLID_BREP ( 'Cut-Extrude1', #5716 ) ;
#9674=EDGE_CURVE ( 'NONE', #5643, #5737, #7861, .T. ) ;
#9716=DIRECTION ( 'NONE',  ( -0.005235963827121952255, 0.9999862922474493931, -2.738476122049126182E-14 ) ) ;
#9803=CARTESIAN_POINT ( 'NONE',  ( -70.63306599754589854, 6.130251853413639651, 3.000000000000100364 ) ) ;
#9953=CARTESIAN_POINT ( 'NONE',  ( -30.79248430819469817, 6.338858557518999959, 5.500000000000089706 ) ) ;
#9956=ORIENTED_EDGE ( 'NONE', *, *, #13236, .F. ) ;
#10045=CYLINDRICAL_SURFACE ( 'NONE', #22274, 3.499999999999998224 ) ;
#10104=EDGE_LOOP ( 'NONE', ( #12245, #8056, #8173, #28 ) ) ;
#10124=ADVANCED_FACE ( 'NONE', ( #18967 ), #17189, .F. ) ;
#10150=EDGE_CURVE ( 'NONE', #12003, #22438, #2464, .T. ) ;
#10235=EDGE_CURVE ( 'NONE', #6625, #12797, #15567, .T. ) ;
#10374=FACE_OUTER_BOUND ( 'NONE', #10104, .T. ) ;
#10398=DIRECTION ( 'NONE',  ( 0.005235963827101452160, -0.9999862922474493931, 5.479105319409471602E-16 ) ) ;
#10423=VECTOR ( 'NONE', #18717, 1000.000000000000000 ) ;
#10462=CARTESIAN_POINT ( 'NONE',  ( 0.03403376487640599746, -6.499910899608420500, 8.873528816395729098E-14 ) ) ;
#10477=DIRECTION ( 'NONE',  ( -1.466984912809907930E-16, -2.805478249466195144E-20, -1.000000000000000000 ) ) ;
#10489=EDGE_LOOP ( 'NONE', ( #16813, #1753, #14748, #17832 ) ) ;
#10579=AXIS2_PLACEMENT_3D ( 'NONE', #2610, #2127, #20538 ) ;
#10590=DIRECTION ( 'NONE',  ( -0.9999862922474492821, -0.005235963827121953122, 1.466966272682004590E-16 ) ) ;
#10604=EDGE_LOOP ( 'NONE', ( #22669, #11011, #18486, #6287 ) ) ;
#10667=APPLICATION_CONTEXT ( 'configuration controlled 3d designs of mechanical parts and assemblies' ) ;
#10687=DIRECTION ( 'NONE',  ( -0.9999862922474492821, -0.005235963827121822151, 1.466966272681990292E-16 ) ) ;
#10705=CARTESIAN_POINT ( 'NONE',  ( -3.499952022866071211, -0.01832587339492825623, 8.925353670776949322E-14 ) ) ;
#10769=EDGE_LOOP ( 'NONE', ( #20197, #4650 ) ) ;
#10850=CARTESIAN_POINT ( 'NONE',  ( -28.52462712253550237, 6.350733138482030249, 0.7325259402521719920 ) ) ;
#10860=AXIS2_PLACEMENT_3D ( 'NONE', #7798, #9716, #16566 ) ;
#11011=ORIENTED_EDGE ( 'NONE', *, *, #22775, .F. ) ;
#11035=CYLINDRICAL_SURFACE ( 'NONE', #17142, 2.500999999999819590 ) ;
#11080=VECTOR ( 'NONE', #10687, 1000.000000000000114 ) ;
#11202=EDGE_LOOP ( 'NONE', ( #6, #13094, #6502, #18965 ) ) ;
#11261=FACE_OUTER_BOUND ( 'NONE', #13717, .T. ) ;
#11314=ORIENTED_EDGE ( 'NONE', *, *, #7006, .T. ) ;
#11367=ADVANCED_BREP_SHAPE_REPRESENTATION ( '', ( #9662, #12739 ), #23107 ) ;
#11479=DIRECTION ( 'NONE',  ( -0.005235963827121941846, 0.9999862922474492821, 7.400535959148351896E-19 ) ) ;
#11532=VERTEX_POINT ( 'NONE', #21603 ) ;
#11649=DIRECTION ( 'NONE',  ( -0.9999862922474492821, -0.005235963827122071951, 1.466966272681990292E-16 ) ) ;
#11659=CYLINDRICAL_SURFACE ( 'NONE', #10579, 0.0009999999999615351298 ) ;
#11676=ADVANCED_FACE ( 'NONE', ( #5826 ), #11659, .F. ) ;
#11705=DIRECTION ( 'NONE',  ( 1.466984912809907930E-16, 2.805478249466195144E-20, 1.000000000000000000 ) ) ;
#11743=CARTESIAN_POINT ( 'NONE',  ( -66.29618031796869104, -0.3471291603817620031, 3.000000000000100364 ) ) ;
#11802=ORIENTED_EDGE ( 'NONE', *, *, #1863, .F. ) ;
#11818=CARTESIAN_POINT ( 'NONE',  ( 5.026060663935580067E-16, -1.434026569662460006E-15, 2.500000000000090150 ) ) ;
#11867=ORIENTED_EDGE ( 'NONE', *, *, #7083, .F. ) ;
#11958=DIRECTION ( 'NONE',  ( 0.005235963827102643048, -0.9999862922474495042, 7.723249237701186312E-15 ) ) ;
#11959=EDGE_LOOP ( 'NONE', ( #18947, #8660, #19266, #16479 ) ) ;
#11984=DIRECTION ( 'NONE',  ( 0.9999862922474492821, 0.005235963827122071951, -1.466966272681990292E-16 ) ) ;
#11999=DIRECTION ( 'NONE',  ( -0.005235963827101446089, 0.9999862922474493931, 7.400535959109775519E-19 ) ) ;
#12003=VERTEX_POINT ( 'NONE', #4359 ) ;
#12016=SHAPE_DEFINITION_REPRESENTATION ( #1306, #20817 ) ;
#12100=CARTESIAN_POINT ( 'NONE',  ( -26.75617730459320143, 6.359992804688680224, 9.266501092714649290E-14 ) ) ;
#12160=DIRECTION ( 'NONE',  ( -0.005235963827104182615, 0.9999862922474495042, 7.400535959114223454E-19 ) ) ;
#12222=AXIS2_PLACEMENT_3D ( 'NONE', #17086, #17223, #21115 ) ;
#12245=ORIENTED_EDGE ( 'NONE', *, *, #19093, .T. ) ;
#12301=DIRECTION ( 'NONE',  ( 0.005235963827063078342, -0.9999862922474496152, 2.538154295128170621E-14 ) ) ;
#12307=AXIS2_PLACEMENT_3D ( 'NONE', #19604, #17607, #14256 ) ;
#12340=EDGE_CURVE ( 'NONE', #16889, #22403, #18112, .T. ) ;
#12454=ADVANCED_FACE ( 'NONE', ( #3970 ), #734, .T. ) ;
#12455=ADVANCED_FACE ( 'NONE', ( #22128 ), #7888, .F. ) ;
#12473=VERTEX_POINT ( 'NONE', #14891 ) ;
#12493=EDGE_LOOP ( 'NONE', ( #13279, #17949, #8057, #3341 ) ) ;
#12522=UNCERTAINTY_MEASURE_WITH_UNIT (LENGTH_MEASURE( 1.000000000000000082E-05 ), #18441, 'distance_accuracy_value', 'NONE');
#12556=EDGE_CURVE ( 'NONE', #22403, #3079, #7516, .T. ) ;
#12613=CARTESIAN_POINT ( 'NONE',  ( -26.68810977484059777, -6.639828994528089723, 2.501000000000090484 ) ) ;
#12662=LINE ( 'NONE', #12876, #16816 ) ;
#12676=CARTESIAN_POINT ( 'NONE',  ( 1.358598381910800010E-16, -1.434096706618689895E-15, 8.874009851233079243E-14 ) ) ;
#12739=AXIS2_PLACEMENT_3D ( 'NONE', #2569, #13380, #415 ) ;
#12763=CARTESIAN_POINT ( 'NONE',  ( -30.72370968135370006, -6.660959539311599897, 2.999707106781279720 ) ) ;
#12797=VERTEX_POINT ( 'NONE', #15940 ) ;
#12819=AXIS2_PLACEMENT_3D ( 'NONE', #18587, #15244, #16542 ) ;
#12838=ORIENTED_EDGE ( 'NONE', *, *, #12556, .F. ) ;
#12856=CARTESIAN_POINT ( 'NONE',  ( -26.68810977484059777, -6.639828994528159889, 2.500000000000090150 ) ) ;
#12876=CARTESIAN_POINT ( 'NONE',  ( -26.68881687192900287, -6.639832696913689603, 2.500292893218909906 ) ) ;
#12911=AXIS2_PLACEMENT_3D ( 'NONE', #5486, #18316, #2040 ) ;
#12935=VECTOR ( 'NONE', #4241, 999.9999999999998863 ) ;
#13047=VECTOR ( 'NONE', #19966, 1000.000000000000114 ) ;
#13049=FACE_OUTER_BOUND ( 'NONE', #10604, .T. ) ;
#13084=VERTEX_POINT ( 'NONE', #4760 ) ;
#13094=ORIENTED_EDGE ( 'NONE', *, *, #14132, .T. ) ;
#13102=LINE ( 'NONE', #8115, #18305 ) ;
#13156=CARTESIAN_POINT ( 'NONE',  ( -22.99995202268987171, -0.1204285676208978334, 9.211416015219178562E-14 ) ) ;
#13162=DIRECTION ( 'NONE',  ( 0.000000000000000000, -6.936119456125000933E-16, -1.000000000000000000 ) ) ;
#13236=EDGE_CURVE ( 'NONE', #489, #7436, #16349, .T. ) ;
#13251=CYLINDRICAL_SURFACE ( 'NONE', #19636, 3.499999999999998668 ) ;
#13268=LINE ( 'NONE', #15515, #12935 ) ;
#13279=ORIENTED_EDGE ( 'NONE', *, *, #22977, .T. ) ;
#13285=ADVANCED_FACE ( 'NONE', ( #3539 ), #7567, .T. ) ;
#13305=VERTEX_POINT ( 'NONE', #7452 ) ;
#13336=CYLINDRICAL_SURFACE ( 'NONE', #1592, 0.0009999999998218898900 ) ;
#13367=CARTESIAN_POINT ( 'NONE',  ( -60.06514239919540188, -6.814592325618320068, 5.500000000000099476 ) ) ;
#13380=DIRECTION ( 'NONE',  ( 0.000000000000000000, 0.000000000000000000, 1.000000000000000000 ) ) ;
#13437=VERTEX_POINT ( 'NONE', #6134 ) ;
#13450=VERTEX_POINT ( 'NONE', #9953 ) ;
#13499=CARTESIAN_POINT ( 'NONE',  ( -26.75617730459320143, 6.359992804688680224, 2.500000000000090150 ) ) ;
#13517=AXIS2_PLACEMENT_3D ( 'NONE', #2391, #21030, #1058 ) ;
#13573=DIRECTION ( 'NONE',  ( 0.000000000000000000, 0.000000000000000000, -1.000000000000000000 ) ) ;
#13586=PLANE ( 'NONE',  #18471 ) ;
#13595=VERTEX_POINT ( 'NONE', #15862 ) ;
#13617=DIRECTION ( 'NONE',  ( 1.000000000000000000, -1.466984912809929871E-16, -5.345529420184390105E-52 ) ) ;
#13672=ORIENTED_EDGE ( 'NONE', *, *, #7445, .T. ) ;
#13717=EDGE_LOOP ( 'NONE', ( #372, #21210, #9380, #2488 ) ) ;
#13782=CIRCLE ( 'NONE', #18727, 6.499999999999997335 ) ;
#13808=EDGE_LOOP ( 'NONE', ( #3408, #5452, #13890, #6310, #18516, #8806, #7731, #9956, #5448, #9414, #2406, #7873 ) ) ;
#13884=PRODUCT_DEFINITION ( 'UNKNOWN', '', #6875, #4942 ) ;
#13890=ORIENTED_EDGE ( 'NONE', *, *, #7006, .F. ) ;
#13894=AXIS2_PLACEMENT_3D ( 'NONE', #16026, #10477, #10590 ) ;
#13896=ORIENTED_EDGE ( 'NONE', *, *, #16160, .F. ) ;
#13969=CARTESIAN_POINT ( 'NONE',  ( -19.49999999982379961, -0.1021026942259709996, 9.160072195675308484E-14 ) ) ;
#13977=VERTEX_POINT ( 'NONE', #20472 ) ;
#14094=CIRCLE ( 'NONE', #12222, 6.499999999999997335 ) ;
#14103=CARTESIAN_POINT ( 'NONE',  ( -3.499952022866071211, -0.01832587339492825623, 8.925353670776949322E-14 ) ) ;
#14132=EDGE_CURVE ( 'NONE', #18750, #12797, #8599, .T. ) ;
#14200=CARTESIAN_POINT ( 'NONE',  ( -0.03403376487617889440, 6.499910899608420500, 2.500000000000090150 ) ) ;
#14215=ORIENTED_EDGE ( 'NONE', *, *, #21811, .T. ) ;
#14256=DIRECTION ( 'NONE',  ( 1.000000000000000000, -1.466984912809909902E-16, 5.345529420184390105E-52 ) ) ;
#14294=EDGE_LOOP ( 'NONE', ( #11802, #22908 ) ) ;
#14322=AXIS2_PLACEMENT_3D ( 'NONE', #11818, #11705, #18824 ) ;
#14449=ADVANCED_FACE ( 'NONE', ( #136 ), #21412, .T. ) ;
#14458=DIRECTION ( 'NONE',  ( 0.005235963827110373843, -0.9999862922474493931, 0.000000000000000000 ) ) ;
#14463=LINE ( 'NONE', #5203, #11080 ) ;
#14465=DIRECTION ( 'NONE',  ( -1.466984912809907930E-16, -2.805478249466190329E-20, -1.000000000000000000 ) ) ;
#14469=CARTESIAN_POINT ( 'NONE',  ( -28.95596696049959817, -6.651703575491109355, 4.767474059747909720 ) ) ;
#14584=FACE_BOUND ( 'NONE', #16357, .T. ) ;
#14637=DIRECTION ( 'NONE',  ( 1.217822455144494161E-14, 0.000000000000000000, 1.000000000000000000 ) ) ;
#14673=ADVANCED_FACE ( 'NONE', ( #9296 ), #16521, .F. ) ;
#14695=EDGE_LOOP ( 'NONE', ( #18887, #9008, #9341, #19427 ) ) ;
#14748=ORIENTED_EDGE ( 'NONE', *, *, #19093, .F. ) ;
#14750=DIRECTION ( 'NONE',  ( -1.466984912809907930E-16, -2.805478249466190329E-20, -1.000000000000000000 ) ) ;
#14820=VERTEX_POINT ( 'NONE', #8330 ) ;
#14891=CARTESIAN_POINT ( 'NONE',  ( -26.75617730459320143, 6.359992804688680224, 9.266501092714649290E-14 ) ) ;
#14936=CARTESIAN_POINT ( 'NONE',  ( -26.72214353971689960, -0.1399180949199889945, 2.500999999999910184 ) ) ;
#14952=CARTESIAN_POINT ( 'NONE',  ( -26.75617730459320143, 6.359992804688680224, 2.500000000000090150 ) ) ;
#15099=ORIENTED_EDGE ( 'NONE', *, *, #1397, .F. ) ;
#15175=VECTOR ( 'NONE', #6072, 999.9999999999998863 ) ;
#15244=DIRECTION ( 'NONE',  ( 0.7070970883417637687, 0.003702385528197202434, 0.7071067811865479058 ) ) ;
#15268=CIRCLE ( 'NONE', #20188, 2.501000000000000334 ) ;
#15306=EDGE_CURVE ( 'NONE', #3681, #7436, #14094, .T. ) ;
#15323=ORIENTED_EDGE ( 'NONE', *, *, #7083, .T. ) ;
#15357=CARTESIAN_POINT ( 'NONE',  ( -19.49999999982379961, -0.1021026942259709996, 9.160072195675308484E-14 ) ) ;
#15359=VECTOR ( 'NONE', #11649, 1000.000000000000114 ) ;
#15368=FACE_OUTER_BOUND ( 'NONE', #12493, .T. ) ;
#15391=DIRECTION ( 'NONE',  ( -1.466984912809907930E-16, -2.805478249466190329E-20, -1.000000000000000000 ) ) ;
#15392=VERTEX_POINT ( 'NONE', #2724 ) ;
#15428=MECHANICAL_CONTEXT ( 'NONE', #10667, 'mechanical' ) ;
#15452=AXIS2_PLACEMENT_3D ( 'NONE', #9318, #10398, #6586 ) ;
#15487=CARTESIAN_POINT ( 'NONE',  ( -28.52462712253550237, 6.350733138482030249, 0.7325259402521709928 ) ) ;
#15494=EDGE_CURVE ( 'NONE', #13437, #3681, #19929, .T. ) ;
#15515=CARTESIAN_POINT ( 'NONE',  ( -30.79177721110609767, 6.338862259904598950, 2.999707106781169585 ) ) ;
#15520=EDGE_CURVE ( 'NONE', #13437, #22247, #14463, .T. ) ;
#15567=CIRCLE ( 'NONE', #20152, 3.499999999999998224 ) ;
#15681=ORIENTED_EDGE ( 'NONE', *, *, #783, .T. ) ;
#15710=CARTESIAN_POINT ( 'NONE',  ( -29.02403449025189985, 6.348118223725100151, 4.767474059747810244 ) ) ;
#15729=ADVANCED_FACE ( 'NONE', ( #13049 ), #11035, .T. ) ;
#15742=ADVANCED_FACE ( 'NONE', ( #14584, #20394, #15368 ), #4121, .T. ) ;
#15765=DIRECTION ( 'NONE',  ( -1.466984912809907930E-16, -2.805478249466190329E-20, -1.000000000000000000 ) ) ;
#15837=DIRECTION ( 'NONE',  ( -1.466984912809907930E-16, -2.805478249466190329E-20, -1.000000000000000000 ) ) ;
#15862=CARTESIAN_POINT ( 'NONE',  ( -30.79248430819469817, 6.338858557518999959, 3.000000000000090150 ) ) ;
#15890=EDGE_LOOP ( 'NONE', ( #2374, #4361, #14215, #12838, #3469, #23184, #1614, #21991, #20958, #3071, #13672, #21772 ) ) ;
#15917=ORIENTED_EDGE ( 'NONE', *, *, #2083, .F. ) ;
#15940=CARTESIAN_POINT ( 'NONE',  ( -16.00004797695772751, -0.08377682083104373567, 9.108728376131438406E-14 ) ) ;
#15981=CARTESIAN_POINT ( 'NONE',  ( -19.49999999982379961, -0.1021026942259709996, 2.500000000000090150 ) ) ;
#16026=CARTESIAN_POINT ( 'NONE',  ( -19.49999999982379961, -0.1021026942259709996, 9.160072195675308484E-14 ) ) ;
#16029=EDGE_CURVE ( 'NONE', #8698, #7573, #5610, .T. ) ;
#16135=EDGE_LOOP ( 'NONE', ( #17520, #15917 ) ) ;
#16160=EDGE_CURVE ( 'NONE', #5502, #13450, #13102, .T. ) ;
#16272=AXIS2_PLACEMENT_3D ( 'NONE', #12676, #19910, #4102 ) ;
#16349=LINE ( 'NONE', #8898, #5635 ) ;
#16357=EDGE_LOOP ( 'NONE', ( #6019, #11867 ) ) ;
#16417=AXIS2_PLACEMENT_3D ( 'NONE', #19655, #2065, #18003 ) ;
#16421=EDGE_LOOP ( 'NONE', ( #3739, #17809, #19188, #15681 ) ) ;
#16431=CARTESIAN_POINT ( 'NONE',  ( 0.03403376487640639991, -6.499910899608420500, 2.500000000000090150 ) ) ;
#16452=DIRECTION ( 'NONE',  ( 0.005235963827101452160, -0.9999862922474493931, 5.479105319409471602E-16 ) ) ;
#16479=ORIENTED_EDGE ( 'NONE', *, *, #12340, .T. ) ;
#16521=CYLINDRICAL_SURFACE ( 'NONE', #6362, 3.499999999999998224 ) ;
#16542=DIRECTION ( 'NONE',  ( 0.005235963827110361700, -0.9999862922474493931, 0.000000000000000000 ) ) ;
#16561=CARTESIAN_POINT ( 'NONE',  ( 1.358598381910800010E-16, -1.434096706618689895E-15, 8.874009851233079243E-14 ) ) ;
#16566=DIRECTION ( 'NONE',  ( 0.000000000000000000, 0.000000000000000000, -1.000000000000000000 ) ) ;
#16574=VECTOR ( 'NONE', #18465, 1000.000000000000114 ) ;
#16669=CARTESIAN_POINT ( 'NONE',  ( -16.00004797695772751, -0.08377682083104373567, 2.500000000000089706 ) ) ;
#16694=DIRECTION ( 'NONE',  ( 4.115594265179474725E-36, 2.805478249463630046E-20, 1.000000000000000000 ) ) ;
#16707=CIRCLE ( 'NONE', #2746, 3.499999999999998224 ) ;
#16757=ORIENTED_EDGE ( 'NONE', *, *, #3297, .T. ) ;
#16758=AXIS2_PLACEMENT_3D ( 'NONE', #431, #1992, #13162 ) ;
#16776=EDGE_LOOP ( 'NONE', ( #2490, #2216, #8813, #20036 ) ) ;
#16813=ORIENTED_EDGE ( 'NONE', *, *, #15306, .F. ) ;
#16816=VECTOR ( 'NONE', #21892, 1000.000000000000114 ) ;
#16889=VERTEX_POINT ( 'NONE', #1164 ) ;
#16960=LINE ( 'NONE', #14952, #15359 ) ;
#16968=EDGE_CURVE ( 'NONE', #13084, #19582, #3419, .T. ) ;
#17012=FACE_OUTER_BOUND ( 'NONE', #16421, .T. ) ;
#17086=CARTESIAN_POINT ( 'NONE',  ( 1.137438022745850001E-13, -8.410916347709809861E-16, 2.500000000000090150 ) ) ;
#17124=ORIENTED_EDGE ( 'NONE', *, *, #12556, .T. ) ;
#17142=AXIS2_PLACEMENT_3D ( 'NONE', #14936, #21814, #7351 ) ;
#17189=PLANE ( 'NONE',  #18240 ) ;
#17223=DIRECTION ( 'NONE',  ( 1.466984912809909902E-16, 2.805478249466345005E-20, 1.000000000000000000 ) ) ;
#17262=EDGE_LOOP ( 'NONE', ( #20660, #2020, #1103, #6631 ) ) ;
#17489=VECTOR ( 'NONE', #8165, 999.9999999999998863 ) ;
#17520=ORIENTED_EDGE ( 'NONE', *, *, #10235, .F. ) ;
#17542=LINE ( 'NONE', #12100, #9527 ) ;
#17543=ADVANCED_FACE ( 'NONE', ( #1313, #8691, #10374 ), #3578, .F. ) ;
#17607=DIRECTION ( 'NONE',  ( 4.115594265186587621E-36, 2.805478249468460519E-20, 1.000000000000000000 ) ) ;
#17743=LINE ( 'NONE', #20939, #21610 ) ;
#17748=DIRECTION ( 'NONE',  ( 1.000000000000000000, -1.466984912809909902E-16, 5.345529420184390105E-52 ) ) ;
#17805=ORIENTED_EDGE ( 'NONE', *, *, #21080, .F. ) ;
#17809=ORIENTED_EDGE ( 'NONE', *, *, #7445, .F. ) ;
#17832=ORIENTED_EDGE ( 'NONE', *, *, #13236, .T. ) ;
#17843=CARTESIAN_POINT ( 'NONE',  ( -69.88753305544580030, 2.884110939634079607, 5.500000000000099476 ) ) ;
#17875=FACE_OUTER_BOUND ( 'NONE', #25, .T. ) ;
#17895=CARTESIAN_POINT ( 'NONE',  ( 1.358598381910800010E-16, -1.434096706618689895E-15, 8.874009851233079243E-14 ) ) ;
#17949=ORIENTED_EDGE ( 'NONE', *, *, #16029, .T. ) ;
#18003=DIRECTION ( 'NONE',  ( 0.000000000000000000, -5.527220191599521464E-16, -1.000000000000000000 ) ) ;
#18050=DIRECTION ( 'NONE',  ( 0.000000000000000000, -2.739767185169682068E-14, -1.000000000000000000 ) ) ;
#18112=LINE ( 'NONE', #7310, #664 ) ;
#18199=EDGE_CURVE ( 'NONE', #19582, #13450, #7723, .T. ) ;
#18240=AXIS2_PLACEMENT_3D ( 'NONE', #11743, #2689, #13617 ) ;
#18250=DIRECTION ( 'NONE',  ( -0.9999862922474493931, -0.005235963827116132258, 1.466966272681990539E-16 ) ) ;
#18283=EDGE_CURVE ( 'NONE', #22247, #12473, #2345, .T. ) ;
#18305=VECTOR ( 'NONE', #7626, 1000.000000000000114 ) ;
#18316=DIRECTION ( 'NONE',  ( -0.005235963827121952255, 0.9999862922474493931, -2.738476122049136279E-14 ) ) ;
#18402=EDGE_LOOP ( 'NONE', ( #19667, #15323, #16757, #19410 ) ) ;
#18441=( LENGTH_UNIT ( ) NAMED_UNIT ( * ) SI_UNIT ( .MILLI., .METRE. ) );
#18465=DIRECTION ( 'NONE',  ( 0.9999862922474492821, 0.005235963827121822151, -1.466966272681990292E-16 ) ) ;
#18471=AXIS2_PLACEMENT_3D ( 'NONE', #1451, #12301, #2787 ) ;
#18486=ORIENTED_EDGE ( 'NONE', *, *, #18283, .F. ) ;
#18487=DIRECTION ( 'NONE',  ( -1.466984912809907930E-16, -2.805478249466190329E-20, -1.000000000000000000 ) ) ;
#18516=ORIENTED_EDGE ( 'NONE', *, *, #783, .F. ) ;
#18587=CARTESIAN_POINT ( 'NONE',  ( -28.52462712253550237, 6.350733138482030249, 0.7325259402521719920 ) ) ;
#18608=CARTESIAN_POINT ( 'NONE',  ( -69.90454993788389970, 6.134066389438220135, 3.000000000000100364 ) ) ;
#18623=CARTESIAN_POINT ( 'NONE',  ( -66.29618031796869104, -0.3471291603817620031, 5.500000000000099476 ) ) ;
#18677=( NAMED_UNIT ( * ) PLANE_ANGLE_UNIT ( ) SI_UNIT ( $, .RADIAN. ) );
#18684=VECTOR ( 'NONE', #20094, 1000.000000000000114 ) ;
#18717=DIRECTION ( 'NONE',  ( 0.9999862922474493931, 0.005235963827116132258, -1.466966272681990539E-16 ) ) ;
#18727=AXIS2_PLACEMENT_3D ( 'NONE', #5151, #23071, #6829 ) ;
#18750=VERTEX_POINT ( 'NONE', #16669 ) ;
#18824=DIRECTION ( 'NONE',  ( -0.9999862922474492821, -0.005235963827121951387, 1.239088197126291310E-16 ) ) ;
#18887=ORIENTED_EDGE ( 'NONE', *, *, #9674, .F. ) ;
#18947=ORIENTED_EDGE ( 'NONE', *, *, #3530, .F. ) ;
#18965=ORIENTED_EDGE ( 'NONE', *, *, #3297, .F. ) ;
#18967=FACE_OUTER_BOUND ( 'NONE', #19259, .T. ) ;
#19093=EDGE_CURVE ( 'NONE', #489, #13437, #13782, .T. ) ;
#19188=ORIENTED_EDGE ( 'NONE', *, *, #9674, .T. ) ;
#19248=AXIS2_PLACEMENT_3D ( 'NONE', #4330, #1086, #13573 ) ;
#19259=EDGE_LOOP ( 'NONE', ( #22665, #5150, #5767, #8201 ) ) ;
#19266=ORIENTED_EDGE ( 'NONE', *, *, #4139, .T. ) ;
#19410=ORIENTED_EDGE ( 'NONE', *, *, #10235, .T. ) ;
#19412=CARTESIAN_POINT ( 'NONE',  ( -26.75688440168130100, 6.359989102302520791, 2.500292893218799772 ) ) ;
#19427=ORIENTED_EDGE ( 'NONE', *, *, #23469, .T. ) ;
#19448=CYLINDRICAL_SURFACE ( 'NONE', #6921, 3.499999999999998668 ) ;
#19525=LINE ( 'NONE', #15487, #21718 ) ;
#19572=DIRECTION ( 'NONE',  ( 1.466984912809907930E-16, 2.805478249466195144E-20, 1.000000000000000000 ) ) ;
#19582=VERTEX_POINT ( 'NONE', #15710 ) ;
#19604=CARTESIAN_POINT ( 'NONE',  ( -11.34268231757140022, -0.05939068843019999766, 9.040405456159088690E-14 ) ) ;
#19636=AXIS2_PLACEMENT_3D ( 'NONE', #16561, #18487, #7442 ) ;
#19645=ORIENTED_EDGE ( 'NONE', *, *, #20238, .F. ) ;
#19655=CARTESIAN_POINT ( 'NONE',  ( -30.75845054331819739, -0.1610523420890130064, 2.999000000000090260 ) ) ;
#19667=ORIENTED_EDGE ( 'NONE', *, *, #14132, .F. ) ;
#19683=AXIS2_PLACEMENT_3D ( 'NONE', #22474, #2645, #6221 ) ;
#19910=DIRECTION ( 'NONE',  ( -1.466984912809907930E-16, -2.805478249466195144E-20, -1.000000000000000000 ) ) ;
#19912=APPLICATION_CONTEXT ( 'configuration controlled 3d designs of mechanical parts and assemblies' ) ;
#19929=LINE ( 'NONE', #10462, #37 ) ;
#19966=DIRECTION ( 'NONE',  ( -0.7070970883417637687, -0.003702385528188433840, 0.7071067811865477948 ) ) ;
#20001=AXIS2_PLACEMENT_3D ( 'NONE', #21924, #72, #14458 ) ;
#20006=CYLINDRICAL_SURFACE ( 'NONE', #16417, 2.500999999999959922 ) ;
#20036=ORIENTED_EDGE ( 'NONE', *, *, #1863, .T. ) ;
#20056=ADVANCED_FACE ( 'NONE', ( #8536 ), #19448, .F. ) ;
#20094=DIRECTION ( 'NONE',  ( 0.005235963827121951387, -0.9999862922474492821, -7.400535959139851804E-19 ) ) ;
#20152=AXIS2_PLACEMENT_3D ( 'NONE', #13969, #21327, #21443 ) ;
#20188=AXIS2_PLACEMENT_3D ( 'NONE', #12613, #5129, #3582 ) ;
#20197=ORIENTED_EDGE ( 'NONE', *, *, #22651, .F. ) ;
#20238=EDGE_CURVE ( 'NONE', #13084, #5502, #22085, .T. ) ;
#20393=CARTESIAN_POINT ( 'NONE',  ( -60.06514239919540188, -6.814592325618320068, 3.000000000000100364 ) ) ;
#20394=FACE_BOUND ( 'NONE', #10769, .T. ) ;
#20395=CARTESIAN_POINT ( 'NONE',  ( -69.88753305544580030, 2.884110939634079607, 3.000000000000100364 ) ) ;
#20472=CARTESIAN_POINT ( 'NONE',  ( -3.499952022866070767, -0.01832587339492825623, 2.500000000000090594 ) ) ;
#20538=DIRECTION ( 'NONE',  ( 0.000000000000000000, 0.000000000000000000, -1.000000000000000000 ) ) ;
#20614=LINE ( 'NONE', #13367, #4138 ) ;
#20660=ORIENTED_EDGE ( 'NONE', *, *, #9286, .F. ) ;
#20817=SHAPE_REPRESENTATION ( '1602p_c_08', ( #12739 ), #23107 ) ;
#20939=CARTESIAN_POINT ( 'NONE',  ( -69.90454993788326021, 6.134066389438223688, -0.7502499999999080460 ) ) ;
#20958=ORIENTED_EDGE ( 'NONE', *, *, #22462, .F. ) ;
#21030=DIRECTION ( 'NONE',  ( -1.466984912809907930E-16, -2.805478249466195144E-20, -1.000000000000000000 ) ) ;
#21080=EDGE_CURVE ( 'NONE', #13305, #8538, #6577, .T. ) ;
#21115=DIRECTION ( 'NONE',  ( -0.005235963827121941846, 0.9999862922474492821, 0.000000000000000000 ) ) ;
#21210=ORIENTED_EDGE ( 'NONE', *, *, #10150, .T. ) ;
#21327=DIRECTION ( 'NONE',  ( -1.466984912809907930E-16, -2.805478249466195144E-20, -1.000000000000000000 ) ) ;
#21331=DIRECTION ( 'NONE',  ( -0.9999862922474492821, -0.005235963827121953122, 1.239088197126291310E-16 ) ) ;
#21412=PLANE ( 'NONE',  #7854 ) ;
#21430=CIRCLE ( 'NONE', #4379, 2.500999999999639734 ) ;
#21443=DIRECTION ( 'NONE',  ( -0.9999862922474492821, -0.005235963827121953122, 1.466966272682004590E-16 ) ) ;
#21570=CARTESIAN_POINT ( 'NONE',  ( -69.90454993788326021, 6.134066389438223688, 5.500000000000099476 ) ) ;
#21603=CARTESIAN_POINT ( 'NONE',  ( -69.83648240813081998, -6.865755409778319773, 3.000000000000100364 ) ) ;
#21610=VECTOR ( 'NONE', #22707, 1000.000000000000000 ) ;
#21625=VECTOR ( 'NONE', #15391, 1000.000000000000000 ) ;
#21718=VECTOR ( 'NONE', #11958, 999.9999999999998863 ) ;
#21742=ADVANCED_FACE ( 'NONE', ( #22524 ), #8164, .T. ) ;
#21772=ORIENTED_EDGE ( 'NONE', *, *, #20238, .T. ) ;
#21811=EDGE_CURVE ( 'NONE', #11532, #3079, #5907, .T. ) ;
#21814=DIRECTION ( 'NONE',  ( -0.005235963827121952255, 0.9999862922474493931, -2.738476122049126182E-14 ) ) ;
#21892=DIRECTION ( 'NONE',  ( -0.7070970883417637687, -0.003702385528188433840, 0.7071067811865477948 ) ) ;
#21924=CARTESIAN_POINT ( 'NONE',  ( -69.87051617300704720, -0.3658445101694126067, 0.000000000000000000 ) ) ;
#21977=DIRECTION ( 'NONE',  ( -0.9999862922474492821, -0.005235963827121953122, 1.466966272682004590E-16 ) ) ;
#21991=ORIENTED_EDGE ( 'NONE', *, *, #15494, .T. ) ;
#22085=CIRCLE ( 'NONE', #23224, 2.501000000000000334 ) ;
#22128=FACE_OUTER_BOUND ( 'NONE', #11959, .T. ) ;
#22214=DIRECTION ( 'NONE',  ( 1.328968407691592047E-16, -2.538119502737155889E-14, -1.000000000000000000 ) ) ;
#22247=VERTEX_POINT ( 'NONE', #7080 ) ;
#22274=AXIS2_PLACEMENT_3D ( 'NONE', #15357, #2535, #974 ) ;
#22292=CARTESIAN_POINT ( 'NONE',  ( -19.49999999982379961, -0.1021026942259709996, 2.500000000000090150 ) ) ;
#22337=FACE_OUTER_BOUND ( 'NONE', #14695, .T. ) ;
#22373=VECTOR ( 'NONE', #22214, 1000.000000000000000 ) ;
#22403=VERTEX_POINT ( 'NONE', #12763 ) ;
#22438=VERTEX_POINT ( 'NONE', #1937 ) ;
#22462=EDGE_CURVE ( 'NONE', #7573, #3681, #7646, .T. ) ;
#22474=CARTESIAN_POINT ( 'NONE',  ( -26.68881687192900287, -6.639832696913689603, 2.500292893218909906 ) ) ;
#22524=FACE_OUTER_BOUND ( 'NONE', #4477, .T. ) ;
#22597=CARTESIAN_POINT ( 'NONE',  ( -11.34268231757140022, -0.05939068843019999766, 2.500000000000090150 ) ) ;
#22651=EDGE_CURVE ( 'NONE', #13977, #12003, #7885, .T. ) ;
#22665=ORIENTED_EDGE ( 'NONE', *, *, #3611, .F. ) ;
#22669=ORIENTED_EDGE ( 'NONE', *, *, #4139, .F. ) ;
#22688=ADVANCED_FACE ( 'NONE', ( #4786 ), #10045, .F. ) ;
#22707=DIRECTION ( 'NONE',  ( 3.338698890017581616E-19, -6.376386915953721864E-17, 1.000000000000000000 ) ) ;
#22775=EDGE_CURVE ( 'NONE', #12473, #1257, #21430, .T. ) ;
#22894=DIRECTION ( 'NONE',  ( -1.466984912809907930E-16, -2.805478249466190329E-20, -1.000000000000000000 ) ) ;
#22897=LINE ( 'NONE', #6511, #3181 ) ;
#22908=ORIENTED_EDGE ( 'NONE', *, *, #5345, .F. ) ;
#22977=EDGE_CURVE ( 'NONE', #7436, #8698, #16960, .T. ) ;
#23057=CARTESIAN_POINT ( 'NONE',  ( -26.75617730459320143, 6.359992804688110901, 2.500999999999740098 ) ) ;
#23071=DIRECTION ( 'NONE',  ( -1.466984912809909902E-16, -2.805478249466345005E-20, -1.000000000000000000 ) ) ;
#23073=CARTESIAN_POINT ( 'NONE',  ( -26.68881687192900287, -6.639832696913689603, 2.500292893218909906 ) ) ;
#23074=ORIENTED_EDGE ( 'NONE', *, *, #8368, .T. ) ;
#23093=DIRECTION ( 'NONE',  ( 1.466984912809907930E-16, 2.805478249466195144E-20, 1.000000000000000000 ) ) ;
#23107=( GEOMETRIC_REPRESENTATION_CONTEXT ( 3 ) GLOBAL_UNCERTAINTY_ASSIGNED_CONTEXT ( ( #12522 ) ) GLOBAL_UNIT_ASSIGNED_CONTEXT ( ( #18441, #18677, #3806 ) ) REPRESENTATION_CONTEXT ( 'NONE', 'WORKASPACE' ) );
#23111=DIRECTION ( 'NONE',  ( -0.9999862922474492821, -0.005235963827121951387, 1.239088197126291310E-16 ) ) ;
#23134=CIRCLE ( 'NONE', #12911, 0.0009999999999996990463 ) ;
#23166=EDGE_CURVE ( 'NONE', #13977, #2098, #4730, .T. ) ;
#23184=ORIENTED_EDGE ( 'NONE', *, *, #4749, .F. ) ;
#23224=AXIS2_PLACEMENT_3D ( 'NONE', #1962, #16452, #7440 ) ;
#23469=EDGE_CURVE ( 'NONE', #8698, #5737, #4763, .T. ) ;
#23543=COLOUR_RGB('Light Gray', 0.72549020, 0.75294118, 0.79215686);
#23544=FILL_AREA_STYLE_COLOUR('',#23543);
#23545=FILL_AREA_STYLE('',(#23544));
#23546=SURFACE_STYLE_FILL_AREA(#23545);
#23547=SURFACE_SIDE_STYLE('',(#23546));
#23548=SURFACE_STYLE_USAGE(.BOTH.,#23547);
#23549=PRESENTATION_STYLE_ASSIGNMENT((#23548));
#23587=STYLED_ITEM('',(#23549),#9662);
#23588=MECHANICAL_DESIGN_GEOMETRIC_PRESENTATION_REPRESENTATION('',(#23587),#23107);
ENDSEC;
END-ISO-10303-21;
